ISO-10303-21;
HEADER;
FILE_DESCRIPTION (('STEP AP214'),
    '1' );
FILE_NAME ('socket head cap screw_am_B18.3.1M - 10 x 1.5 x 70 Hex SHCS -- 32NHX.step',
    '2026-10-28T15:55:38',
    ( '' ),
    ( '' ),
    'SwSTEP 2.0',
    'SolidWorks 2025',
    '' );
FILE_SCHEMA (( 'AUTOMOTIVE_DESIGN' ));
ENDSEC;

DATA;
#10=DIRECTION ( 'NONE',  ( 0.000000000000000000, -9.256405414277014607E-16, -1.000000000000000000 ) ) ;
#12=DIRECTION ( 'NONE',  ( 0.000000000000000000, -0.5000000000000011102, -0.8660254037844379305 ) ) ;
#15=VERTEX_POINT ( 'NONE', #5559 ) ;
#21=AXIS2_PLACEMENT_3D ( 'NONE', #2988, #8149, #4924 ) ;
#25=PLANE ( 'NONE',  #834 ) ;
#71=ORIENTED_EDGE ( 'NONE', *, *, #7854, .T. ) ;
#81=CARTESIAN_POINT ( 'NONE',  ( 5.000000000000000000, -4.685197434473809430, 7.372574772901430151E-15 ) ) ;
#89=ORIENTED_EDGE ( 'NONE', *, *, #6806, .F. ) ;
#90=CARTESIAN_POINT ( 'NONE',  ( 0.000000000000000000, 4.685197434473814759, -5.637851296924623057E-15 ) ) ;
#92=CIRCLE ( 'NONE', #4811, 8.000000000000000000 ) ;
#130=DIRECTION ( 'NONE',  ( 0.000000000000000000, 0.8660254037844380415, -0.5000000000000011102 ) ) ;
#139=CARTESIAN_POINT ( 'NONE',  ( 9.999999999999998224, 6.613092715395750854E-16, 5.400000000000035882 ) ) ;
#143=ORIENTED_EDGE ( 'NONE', *, *, #7822, .F. ) ;
#146=DIRECTION ( 'NONE',  ( -1.000000000000000000, -0.000000000000000000, -0.000000000000000000 ) ) ;
#155=CIRCLE ( 'NONE', #163, 6.999999999999999112 ) ;
#163=AXIS2_PLACEMENT_3D ( 'NONE', #406, #5689, #1262 ) ;
#206=CARTESIAN_POINT ( 'NONE',  ( -31.74999999999995737, 0.000000000000000000, 0.000000000000000000 ) ) ;
#212=CARTESIAN_POINT ( 'NONE',  ( 4.999999999999994671, 0.000000000000000000, 4.057500000000000107 ) ) ;
#213=CARTESIAN_POINT ( 'NONE',  ( 0.000000000000000000, 2.342598717236902939, -4.057500000000001883 ) ) ;
#216=DIRECTION ( 'NONE',  ( 0.000000000000000000, 0.000000000000000000, 1.000000000000000000 ) ) ;
#234=EDGE_LOOP ( 'NONE', ( #3769, #1956 ) ) ;
#238=CARTESIAN_POINT ( 'NONE',  ( 4.999999999999994671, 0.000000000000000000, 0.000000000000000000 ) ) ;
#239=SHAPE_REPRESENTATION ( 'socket head cap screw_am_B18.3.1M - 10 x 1.5 x 70 Hex SHCS -- 32NHX', ( #1299 ), #3819 ) ;
#249=LINE ( 'NONE', #7309, #1348 ) ;
#250=CONICAL_SURFACE ( 'NONE', #6332, 6.999999999999999112, 0.7853981633974482790 ) ;
#328=DIRECTION ( 'NONE',  ( 0.000000000000000000, 0.000000000000000000, -1.000000000000000000 ) ) ;
#332=ORIENTED_EDGE ( 'NONE', *, *, #3253, .T. ) ;
#349=ORIENTED_EDGE ( 'NONE', *, *, #2079, .F. ) ;
#362=ORIENTED_EDGE ( 'NONE', *, *, #3599, .T. ) ;
#406=CARTESIAN_POINT ( 'NONE',  ( 0.000000000000000000, 0.000000000000000000, 0.000000000000000000 ) ) ;
#408=DIRECTION ( 'NONE',  ( 0.000000000000000000, -1.000000000000000000, 0.000000000000000000 ) ) ;
#413=CIRCLE ( 'NONE', #1506, 4.057500000000000107 ) ;
#414=ORIENTED_EDGE ( 'NONE', *, *, #7854, .F. ) ;
#417=PLANE ( 'NONE',  #21 ) ;
#434=CIRCLE ( 'NONE', #1525, 0.4000000000000001887 ) ;
#456=ORIENTED_EDGE ( 'NONE', *, *, #6488, .T. ) ;
#463=ORIENTED_EDGE ( 'NONE', *, *, #6488, .F. ) ;
#480=EDGE_LOOP ( 'NONE', ( #1640, #5852, #3435, #5019 ) ) ;
#487=DIRECTION ( 'NONE',  ( 1.000000000000000000, 0.000000000000000000, 0.000000000000000000 ) ) ;
#490=LINE ( 'NONE', #5647, #5836 ) ;
#502=DIRECTION ( 'NONE',  ( 0.000000000000000000, 0.000000000000000000, 1.000000000000000000 ) ) ;
#511=DIRECTION ( 'NONE',  ( 0.000000000000000000, 0.5000000000000011102, 0.8660254037844380415 ) ) ;
#523=APPLICATION_CONTEXT ( 'automotive_design' ) ;
#540=CIRCLE ( 'NONE', #7016, 5.400000000000035882 ) ;
#562=ADVANCED_FACE ( 'NONE', ( #7966 ), #3422, .T. ) ;
#597=CARTESIAN_POINT ( 'NONE',  ( 5.000000000000000000, -2.342598717236909600, -4.057499999999997442 ) ) ;
#600=CARTESIAN_POINT ( 'NONE',  ( -31.74999999999995737, 6.123233995736809670E-16, -5.000000000000035527 ) ) ;
#626=DIRECTION ( 'NONE',  ( 0.000000000000000000, 0.000000000000000000, -1.000000000000000000 ) ) ;
#628=ORIENTED_EDGE ( 'NONE', *, *, #6965, .T. ) ;
#649=LINE ( 'NONE', #1933, #4243 ) ;
#656=AXIS2_PLACEMENT_3D ( 'NONE', #8184, #408, #2979 ) ;
#665=ADVANCED_FACE ( 'NONE', ( #7284 ), #4016, .F. ) ;
#683=EDGE_LOOP ( 'NONE', ( #5430, #349 ) ) ;
#695=LINE ( 'NONE', #5367, #1574 ) ;
#700=CIRCLE ( 'NONE', #5822, 5.000000000000070166 ) ;
#708=ORIENTED_EDGE ( 'NONE', *, *, #4152, .F. ) ;
#712=DIRECTION ( 'NONE',  ( 1.000000000000000000, 0.000000000000000000, 0.000000000000000000 ) ) ;
#745=CIRCLE ( 'NONE', #1834, 4.057500000000000107 ) ;
#757=ADVANCED_FACE ( 'NONE', ( #3388 ), #6254, .T. ) ;
#767=EDGE_CURVE ( 'NONE', #3292, #4329, #8159, .T. ) ;
#793=VECTOR ( 'NONE', #4334, 1000.000000000000000 ) ;
#800=CIRCLE ( 'NONE', #7265, 5.000000000000035527 ) ;
#834=AXIS2_PLACEMENT_3D ( 'NONE', #2619, #5348, #2002 ) ;
#846=FACE_OUTER_BOUND ( 'NONE', #1424, .T. ) ;
#870=ORIENTED_EDGE ( 'NONE', *, *, #4995, .T. ) ;
#932=VECTOR ( 'NONE', #5994, 1000.000000000000114 ) ;
#935=ORIENTED_EDGE ( 'NONE', *, *, #5323, .F. ) ;
#937=EDGE_CURVE ( 'NONE', #1427, #6149, #2148, .T. ) ;
#939=CIRCLE ( 'NONE', #3766, 6.999999999999999112 ) ;
#943=DIRECTION ( 'NONE',  ( 0.000000000000000000, -0.8660254037844394848, -0.4999999999999985567 ) ) ;
#945=AXIS2_PLACEMENT_3D ( 'NONE', #2136, #943, #2263 ) ;
#949=EDGE_CURVE ( 'NONE', #6896, #7049, #745, .T. ) ;
#950=MANIFOLD_SOLID_BREP ( 'Hex', #5717 ) ;
#970=ORIENTED_EDGE ( 'NONE', *, *, #4796, .F. ) ;
#978=CARTESIAN_POINT ( 'NONE',  ( 9.999999999999998224, 8.000000000000000000, 0.000000000000000000 ) ) ;
#980=EDGE_CURVE ( 'NONE', #6005, #3213, #8251, .T. ) ;
#981=DIRECTION ( 'NONE',  ( 1.000000000000000000, 0.000000000000000000, 0.000000000000000000 ) ) ;
#1007=UNCERTAINTY_MEASURE_WITH_UNIT (LENGTH_MEASURE( 1.000000000000000082E-05 ), #7671, 'distance_accuracy_value', 'NONE');
#1059=FACE_OUTER_BOUND ( 'NONE', #4213, .T. ) ;
#1080=AXIS2_PLACEMENT_3D ( 'NONE', #8213, #3677, #6253 ) ;
#1099=FACE_OUTER_BOUND ( 'NONE', #5566, .T. ) ;
#1106=DIRECTION ( 'NONE',  ( 0.000000000000000000, 0.000000000000000000, 1.000000000000000000 ) ) ;
#1118=AXIS2_PLACEMENT_3D ( 'NONE', #5467, #6003, #2117 ) ;
#1119=PLANE ( 'NONE',  #1080 ) ;
#1136=EDGE_CURVE ( 'NONE', #2735, #2791, #5195, .T. ) ;
#1138=DIRECTION ( 'NONE',  ( 0.000000000000000000, -0.4999999999999985012, 0.8660254037844393737 ) ) ;
#1146=CARTESIAN_POINT ( 'NONE',  ( 4.999999999999994671, 0.000000000000000000, 0.000000000000000000 ) ) ;
#1147=CARTESIAN_POINT ( 'NONE',  ( 10.40000000000000036, 0.000000000000000000, 0.000000000000000000 ) ) ;
#1179=DIRECTION ( 'NONE',  ( 1.000000000000000000, 0.000000000000000000, 0.000000000000000000 ) ) ;
#1186=ORIENTED_EDGE ( 'NONE', *, *, #6072, .T. ) ;
#1201=EDGE_LOOP ( 'NONE', ( #3927, #8317, #362, #71, #6233 ) ) ;
#1241=ORIENTED_EDGE ( 'NONE', *, *, #4266, .F. ) ;
#1255=CARTESIAN_POINT ( 'NONE',  ( 80.00000000000000000, 5.109226446042757607E-16, -4.171999999999999709 ) ) ;
#1257=LINE ( 'NONE', #1984, #2389 ) ;
#1262=DIRECTION ( 'NONE',  ( 0.000000000000000000, 0.000000000000000000, 1.000000000000000000 ) ) ;
#1268=VERTEX_POINT ( 'NONE', #1687 ) ;
#1282=DIRECTION ( 'NONE',  ( 0.000000000000000000, 0.4999999999999984457, -0.8660254037844394848 ) ) ;
#1284=ADVANCED_FACE ( 'NONE', ( #3075, #1059 ), #417, .T. ) ;
#1288=CARTESIAN_POINT ( 'NONE',  ( 4.999999999999994671, 0.000000000000000000, 0.000000000000000000 ) ) ;
#1299=AXIS2_PLACEMENT_3D ( 'NONE', #5884, #1507, #5927 ) ;
#1305=ADVANCED_FACE ( 'NONE', ( #2420 ), #6911, .F. ) ;
#1307=ORIENTED_EDGE ( 'NONE', *, *, #3236, .F. ) ;
#1329=ORIENTED_EDGE ( 'NONE', *, *, #4888, .F. ) ;
#1331=ORIENTED_EDGE ( 'NONE', *, *, #6752, .T. ) ;
#1335=EDGE_CURVE ( 'NONE', #2735, #4851, #7311, .T. ) ;
#1339=AXIS2_PLACEMENT_3D ( 'NONE', #3949, #1467, #3302 ) ;
#1344=ORIENTED_EDGE ( 'NONE', *, *, #6965, .F. ) ;
#1348=VECTOR ( 'NONE', #2178, 1000.000000000000000 ) ;
#1360=ORIENTED_EDGE ( 'NONE', *, *, #1717, .F. ) ;
#1376=ORIENTED_EDGE ( 'NONE', *, *, #1702, .F. ) ;
#1397=DIRECTION ( 'NONE',  ( 0.000000000000000000, 0.000000000000000000, 1.000000000000000000 ) ) ;
#1411=LINE ( 'NONE', #6638, #932 ) ;
#1424=EDGE_LOOP ( 'NONE', ( #7076, #1426, #8158, #1967, #7290 ) ) ;
#1425=FACE_OUTER_BOUND ( 'NONE', #5658, .T. ) ;
#1426=ORIENTED_EDGE ( 'NONE', *, *, #7844, .T. ) ;
#1427=VERTEX_POINT ( 'NONE', #4098 ) ;
#1462=EDGE_CURVE ( 'NONE', #1581, #15, #2602, .T. ) ;
#1463=CARTESIAN_POINT ( 'NONE',  ( 9.999999999999998224, 0.000000000000000000, 0.000000000000000000 ) ) ;
#1467=DIRECTION ( 'NONE',  ( 1.000000000000000000, 0.000000000000000000, 0.000000000000000000 ) ) ;
#1485=EDGE_LOOP ( 'NONE', ( #2510, #7558, #3993, #7342, #2502 ) ) ;
#1493=DIRECTION ( 'NONE',  ( -0.5000000000000042188, 1.060575238724903710E-16, -0.8660254037844361541 ) ) ;
#1506=AXIS2_PLACEMENT_3D ( 'NONE', #1146, #6279, #502 ) ;
#1507=DIRECTION ( 'NONE',  ( 0.000000000000000000, 0.000000000000000000, 1.000000000000000000 ) ) ;
#1516=CARTESIAN_POINT ( 'NONE',  ( 80.00000000000000000, 0.000000000000000000, 0.000000000000000000 ) ) ;
#1525=AXIS2_PLACEMENT_3D ( 'NONE', #2442, #6859, #5595 ) ;
#1529=CARTESIAN_POINT ( 'NONE',  ( 5.000000000000000000, -4.685197434473809430, 7.372574772901430151E-15 ) ) ;
#1532=CARTESIAN_POINT ( 'NONE',  ( 9.999999999999994671, 0.000000000000000000, 0.000000000000000000 ) ) ;
#1537=VERTEX_POINT ( 'NONE', #139 ) ;
#1555=EDGE_CURVE ( 'NONE', #8231, #1537, #434, .T. ) ;
#1574=VECTOR ( 'NONE', #7913, 1000.000000000000114 ) ;
#1578=VECTOR ( 'NONE', #8083, 1000.000000000000000 ) ;
#1581=VERTEX_POINT ( 'NONE', #8261 ) ;
#1603=LINE ( 'NONE', #5604, #3077 ) ;
#1611=CONICAL_SURFACE ( 'NONE', #7408, 4.171999999999999709, 0.7853981633975609666 ) ;
#1638=DIRECTION ( 'NONE',  ( -1.000000000000000000, -0.000000000000000000, -0.000000000000000000 ) ) ;
#1640=ORIENTED_EDGE ( 'NONE', *, *, #1555, .F. ) ;
#1651=DIRECTION ( 'NONE',  ( -1.000000000000000000, -0.000000000000000000, -0.000000000000000000 ) ) ;
#1681=PLANE ( 'NONE',  #3756 ) ;
#1687=CARTESIAN_POINT ( 'NONE',  ( 9.999999999999994671, 9.797174393178825657E-16, -8.000000000000000000 ) ) ;
#1688=VECTOR ( 'NONE', #6126, 1000.000000000000000 ) ;
#1702=EDGE_CURVE ( 'NONE', #1581, #6149, #490, .T. ) ;
#1713=CARTESIAN_POINT ( 'NONE',  ( 80.00000000000000000, 0.000000000000000000, 0.000000000000000000 ) ) ;
#1717=EDGE_CURVE ( 'NONE', #6640, #1836, #155, .T. ) ;
#1732=DIRECTION ( 'NONE',  ( -1.000000000000000000, -0.000000000000000000, -0.000000000000000000 ) ) ;
#1741=ORIENTED_EDGE ( 'NONE', *, *, #2196, .F. ) ;
#1761=VECTOR ( 'NONE', #6971, 1000.000000000000000 ) ;
#1769=FACE_OUTER_BOUND ( 'NONE', #7750, .T. ) ;
#1778=CARTESIAN_POINT ( 'NONE',  ( 5.000000000000000000, 7.027796151710712813, -4.057500000000006324 ) ) ;
#1789=PLANE ( 'NONE',  #4547 ) ;
#1790=PLANE ( 'NONE',  #3594 ) ;
#1834=AXIS2_PLACEMENT_3D ( 'NONE', #3414, #5999, #216 ) ;
#1836=VERTEX_POINT ( 'NONE', #4048 ) ;
#1841=DIRECTION ( 'NONE',  ( 0.000000000000000000, -1.000000000000000000, 9.256405414277014607E-16 ) ) ;
#1851=EDGE_CURVE ( 'NONE', #1836, #2601, #1411, .T. ) ;
#1853=DIRECTION ( 'NONE',  ( 0.000000000000000000, 0.000000000000000000, 1.000000000000000000 ) ) ;
#1870=ORIENTED_EDGE ( 'NONE', *, *, #937, .T. ) ;
#1883=EDGE_LOOP ( 'NONE', ( #3663, #1360, #5279, #4808 ) ) ;
#1900=DIRECTION ( 'NONE',  ( 0.000000000000000000, 0.000000000000000000, -1.000000000000000000 ) ) ;
#1905=CARTESIAN_POINT ( 'NONE',  ( 10.40000000000000036, 0.000000000000000000, 0.000000000000000000 ) ) ;
#1907=EDGE_CURVE ( 'NONE', #5704, #1427, #8347, .T. ) ;
#1916=ORIENTED_EDGE ( 'NONE', *, *, #5562, .T. ) ;
#1933=CARTESIAN_POINT ( 'NONE',  ( 5.000000000000000000, -4.685197434473809430, 7.372574772901430151E-15 ) ) ;
#1941=CARTESIAN_POINT ( 'NONE',  ( 10.40000000000000036, 0.000000000000000000, 5.000000000000035527 ) ) ;
#1956=ORIENTED_EDGE ( 'NONE', *, *, #7898, .T. ) ;
#1967=ORIENTED_EDGE ( 'NONE', *, *, #949, .T. ) ;
#1982=LINE ( 'NONE', #90, #3734 ) ;
#1984=CARTESIAN_POINT ( 'NONE',  ( 5.000000000000000000, 2.342598717236902939, -4.057500000000001883 ) ) ;
#2002=DIRECTION ( 'NONE',  ( 0.000000000000000000, -0.4999999999999984457, 0.8660254037844394848 ) ) ;
#2017=DIRECTION ( 'NONE',  ( -1.000000000000000000, -0.000000000000000000, -0.000000000000000000 ) ) ;
#2023=TOROIDAL_SURFACE ( 'NONE', #3455, 5.400000000000035882, 0.4000000000000000222 ) ;
#2039=ORIENTED_EDGE ( 'NONE', *, *, #5463, .T. ) ;
#2046=DIRECTION ( 'NONE',  ( 0.000000000000000000, 0.000000000000000000, -1.000000000000000000 ) ) ;
#2061=CARTESIAN_POINT ( 'NONE',  ( 9.999999999999994671, 0.000000000000000000, 8.000000000000000000 ) ) ;
#2065=LINE ( 'NONE', #3366, #3354 ) ;
#2079=EDGE_CURVE ( 'NONE', #4329, #3292, #4168, .T. ) ;
#2084=CARTESIAN_POINT ( 'NONE',  ( 80.00000000000000000, 4.171999999999999709, 0.000000000000000000 ) ) ;
#2115=CARTESIAN_POINT ( 'NONE',  ( 79.17200000000011073, 6.123233995736852071E-16, -5.000000000000070166 ) ) ;
#2117=DIRECTION ( 'NONE',  ( 0.000000000000000000, 0.000000000000000000, 1.000000000000000000 ) ) ;
#2121=LINE ( 'NONE', #4668, #5089 ) ;
#2136=CARTESIAN_POINT ( 'NONE',  ( 5.000000000000000000, 4.685197434473814759, -5.637851296924623057E-15 ) ) ;
#2139=ORIENTED_EDGE ( 'NONE', *, *, #1702, .T. ) ;
#2148=LINE ( 'NONE', #7288, #4364 ) ;
#2178=DIRECTION ( 'NONE',  ( -1.000000000000000000, -0.000000000000000000, -0.000000000000000000 ) ) ;
#2196=EDGE_CURVE ( 'NONE', #7049, #1427, #413, .T. ) ;
#2200=DIRECTION ( 'NONE',  ( -1.000000000000000000, -0.000000000000000000, -0.000000000000000000 ) ) ;
#2232=PLANE ( 'NONE',  #2406 ) ;
#2253=ORIENTED_EDGE ( 'NONE', *, *, #8247, .T. ) ;
#2263=DIRECTION ( 'NONE',  ( 0.000000000000000000, 0.4999999999999985012, -0.8660254037844393737 ) ) ;
#2294=EDGE_LOOP ( 'NONE', ( #4985, #8133 ) ) ;
#2311=( LENGTH_UNIT ( ) NAMED_UNIT ( * ) SI_UNIT ( .MILLI., .METRE. ) );
#2327=DIRECTION ( 'NONE',  ( 0.000000000000000000, -0.5000000000000011102, -0.8660254037844379305 ) ) ;
#2335=EDGE_CURVE ( 'NONE', #3678, #2601, #3117, .T. ) ;
#2338=PLANE ( 'NONE',  #7252 ) ;
#2356=FACE_OUTER_BOUND ( 'NONE', #2851, .T. ) ;
#2358=ORIENTED_EDGE ( 'NONE', *, *, #4152, .T. ) ;
#2381=ADVANCED_FACE ( 'NONE', ( #5859 ), #25, .T. ) ;
#2389=VECTOR ( 'NONE', #2521, 1000.000000000000000 ) ;
#2405=CARTESIAN_POINT ( 'NONE',  ( 1.000000000000000888, 9.797174393178827630E-16, 8.000000000000000000 ) ) ;
#2406=AXIS2_PLACEMENT_3D ( 'NONE', #6077, #130, #6040 ) ;
#2409=LINE ( 'NONE', #5050, #7543 ) ;
#2420=FACE_OUTER_BOUND ( 'NONE', #480, .T. ) ;
#2424=FACE_OUTER_BOUND ( 'NONE', #1485, .T. ) ;
#2442=CARTESIAN_POINT ( 'NONE',  ( 10.40000000000000036, 6.613092715395750854E-16, 5.400000000000035882 ) ) ;
#2452=EDGE_CURVE ( 'NONE', #4851, #2735, #700, .T. ) ;
#2453=DIRECTION ( 'NONE',  ( 0.000000000000000000, -0.4999999999999985012, 0.8660254037844393737 ) ) ;
#2475=ORIENTED_EDGE ( 'NONE', *, *, #3825, .F. ) ;
#2479=PRODUCT_DEFINITION_FORMATION_WITH_SPECIFIED_SOURCE ( 'ANY', '', #7427, .NOT_KNOWN. ) ;
#2502=ORIENTED_EDGE ( 'NONE', *, *, #4796, .T. ) ;
#2510=ORIENTED_EDGE ( 'NONE', *, *, #3825, .T. ) ;
#2515=ORIENTED_EDGE ( 'NONE', *, *, #4888, .T. ) ;
#2520=PLANE ( 'NONE',  #5108 ) ;
#2521=DIRECTION ( 'NONE',  ( 0.000000000000000000, -1.000000000000000000, 9.256405414277014607E-16 ) ) ;
#2576=CARTESIAN_POINT ( 'NONE',  ( 5.000000000000000000, -4.685197434473809430, 7.372574772901430151E-15 ) ) ;
#2601=VERTEX_POINT ( 'NONE', #2405 ) ;
#2602=CIRCLE ( 'NONE', #1118, 4.057500000000000107 ) ;
#2604=DIRECTION ( 'NONE',  ( 0.000000000000000000, 1.000000000000000000, -9.256405414277014607E-16 ) ) ;
#2617=DIRECTION ( 'NONE',  ( -1.000000000000000000, -0.000000000000000000, -0.000000000000000000 ) ) ;
#2619=CARTESIAN_POINT ( 'NONE',  ( 5.000000000000000000, -4.685197434473809430, 7.372574772901430151E-15 ) ) ;
#2649=EDGE_CURVE ( 'NONE', #5704, #6005, #7633, .T. ) ;
#2662=DIRECTION ( 'NONE',  ( -1.000000000000000000, -0.000000000000000000, -0.000000000000000000 ) ) ;
#2678=ADVANCED_FACE ( 'NONE', ( #3179 ), #5770, .F. ) ;
#2702=LINE ( 'NONE', #4037, #7554 ) ;
#2720=ORIENTED_EDGE ( 'NONE', *, *, #2079, .T. ) ;
#2727=CARTESIAN_POINT ( 'NONE',  ( -31.74999999999995737, 0.000000000000000000, 0.000000000000000000 ) ) ;
#2730=AXIS2_PLACEMENT_3D ( 'NONE', #4327, #8272, #1853 ) ;
#2735=VERTEX_POINT ( 'NONE', #2115 ) ;
#2736=DIRECTION ( 'NONE',  ( -1.000000000000000000, -0.000000000000000000, -0.000000000000000000 ) ) ;
#2739=CARTESIAN_POINT ( 'NONE',  ( 5.000000000000000000, 4.685197434473814759, -5.637851296924623057E-15 ) ) ;
#2764=EDGE_CURVE ( 'NONE', #3078, #1537, #7927, .T. ) ;
#2771=ORIENTED_EDGE ( 'NONE', *, *, #7745, .F. ) ;
#2785=DIRECTION ( 'NONE',  ( 0.000000000000000000, 0.000000000000000000, -1.000000000000000000 ) ) ;
#2791=VERTEX_POINT ( 'NONE', #7289 ) ;
#2810=DIRECTION ( 'NONE',  ( 0.000000000000000000, 0.000000000000000000, 1.000000000000000000 ) ) ;
#2811=AXIS2_PLACEMENT_3D ( 'NONE', #2084, #712, #2046 ) ;
#2834=DIRECTION ( 'NONE',  ( 0.000000000000000000, 0.000000000000000000, 1.000000000000000000 ) ) ;
#2847=CARTESIAN_POINT ( 'NONE',  ( 80.00000000000000000, 0.000000000000000000, 0.000000000000000000 ) ) ;
#2850=UNCERTAINTY_MEASURE_WITH_UNIT (LENGTH_MEASURE( 1.000000000000000082E-05 ), #2311, 'distance_accuracy_value', 'NONE');
#2851=EDGE_LOOP ( 'NONE', ( #708, #2720, #2956, #6617 ) ) ;
#2861=FACE_OUTER_BOUND ( 'NONE', #2294, .T. ) ;
#2913=ORIENTED_EDGE ( 'NONE', *, *, #767, .T. ) ;
#2925=EDGE_CURVE ( 'NONE', #15, #6775, #7123, .T. ) ;
#2939=DIRECTION ( 'NONE',  ( 1.000000000000000000, 0.000000000000000000, 0.000000000000000000 ) ) ;
#2943=ORIENTED_EDGE ( 'NONE', *, *, #5416, .F. ) ;
#2945=ORIENTED_EDGE ( 'NONE', *, *, #3376, .F. ) ;
#2949=DIRECTION ( 'NONE',  ( 0.000000000000000000, 0.000000000000000000, -1.000000000000000000 ) ) ;
#2952=VERTEX_POINT ( 'NONE', #7185 ) ;
#2956=ORIENTED_EDGE ( 'NONE', *, *, #6806, .T. ) ;
#2979=DIRECTION ( 'NONE',  ( 0.000000000000000000, 0.000000000000000000, -1.000000000000000000 ) ) ;
#2988=CARTESIAN_POINT ( 'NONE',  ( 1.562058576037991531E-17, 0.000000000000000000, 0.000000000000000000 ) ) ;
#3008=FACE_OUTER_BOUND ( 'NONE', #5304, .T. ) ;
#3029=ORIENTED_EDGE ( 'NONE', *, *, #6750, .F. ) ;
#3030=CARTESIAN_POINT ( 'NONE',  ( 4.999999999999994671, 0.000000000000000000, 0.000000000000000000 ) ) ;
#3051=PLANE ( 'NONE',  #945 ) ;
#3052=ORIENTED_EDGE ( 'NONE', *, *, #6423, .F. ) ;
#3066=CARTESIAN_POINT ( 'NONE',  ( 80.00000000000000000, 0.000000000000000000, 4.171999999999999709 ) ) ;
#3075=FACE_BOUND ( 'NONE', #3160, .T. ) ;
#3077=VECTOR ( 'NONE', #4228, 1000.000000000000227 ) ;
#3078=VERTEX_POINT ( 'NONE', #4533 ) ;
#3103=ADVANCED_FACE ( 'NONE', ( #7818 ), #1790, .F. ) ;
#3113=ORIENTED_EDGE ( 'NONE', *, *, #2452, .F. ) ;
#3117=CIRCLE ( 'NONE', #7582, 8.000000000000000000 ) ;
#3160=EDGE_LOOP ( 'NONE', ( #5157, #3998, #628, #7007, #3029, #2475 ) ) ;
#3179=FACE_OUTER_BOUND ( 'NONE', #4817, .T. ) ;
#3191=DIRECTION ( 'NONE',  ( 0.000000000000000000, -1.000000000000000000, 9.256405414277014607E-16 ) ) ;
#3193=AXIS2_PLACEMENT_3D ( 'NONE', #1288, #3856, #2834 ) ;
#3206=ORIENTED_EDGE ( 'NONE', *, *, #3954, .T. ) ;
#3209=DIRECTION ( 'NONE',  ( -1.000000000000000000, -0.000000000000000000, -0.000000000000000000 ) ) ;
#3213=VERTEX_POINT ( 'NONE', #4749 ) ;
#3225=CIRCLE ( 'NONE', #5264, 8.000000000000000000 ) ;
#3232=ADVANCED_FACE ( 'NONE', ( #4106 ), #2023, .F. ) ;
#3236=EDGE_CURVE ( 'NONE', #4851, #8231, #2121, .T. ) ;
#3253=EDGE_CURVE ( 'NONE', #8231, #2791, #6577, .T. ) ;
#3264=ORIENTED_EDGE ( 'NONE', *, *, #937, .F. ) ;
#3288=CARTESIAN_POINT ( 'NONE',  ( 1.000000000000000888, 0.000000000000000000, 0.000000000000000000 ) ) ;
#3292=VERTEX_POINT ( 'NONE', #4829 ) ;
#3293=MECHANICAL_DESIGN_GEOMETRIC_PRESENTATION_REPRESENTATION('',(#7355),#4226);
#3294=LINE ( 'NONE', #1255, #4527 ) ;
#3302=DIRECTION ( 'NONE',  ( 0.000000000000000000, 0.000000000000000000, -1.000000000000000000 ) ) ;
#3305=DIRECTION ( 'NONE',  ( 0.000000000000000000, -0.5000000000000011102, -0.8660254037844379305 ) ) ;
#3330=ORIENTED_EDGE ( 'NONE', *, *, #7745, .T. ) ;
#3354=VECTOR ( 'NONE', #1493, 1000.000000000000114 ) ;
#3355=CARTESIAN_POINT ( 'NONE',  ( 5.000000000000000000, 2.342598717236915373, 4.057499999999997442 ) ) ;
#3356=ORIENTED_EDGE ( 'NONE', *, *, #7989, .T. ) ;
#3357=AXIS2_PLACEMENT_3D ( 'NONE', #5488, #1732, #7514 ) ;
#3366=CARTESIAN_POINT ( 'NONE',  ( 4.999999999999994671, 4.969004387540385421E-16, -4.057500000000000107 ) ) ;
#3376=EDGE_CURVE ( 'NONE', #6775, #3808, #1257, .T. ) ;
#3388=FACE_OUTER_BOUND ( 'NONE', #3458, .T. ) ;
#3407=CARTESIAN_POINT ( 'NONE',  ( 80.00000000000000000, 5.616230220889804839E-16, -4.171999999999999709 ) ) ;
#3414=CARTESIAN_POINT ( 'NONE',  ( 4.999999999999994671, 0.000000000000000000, 0.000000000000000000 ) ) ;
#3422=CYLINDRICAL_SURFACE ( 'NONE', #6936, 5.000000000000035527 ) ;
#3435=ORIENTED_EDGE ( 'NONE', *, *, #5415, .T. ) ;
#3455=AXIS2_PLACEMENT_3D ( 'NONE', #7857, #5311, #8005 ) ;
#3458=EDGE_LOOP ( 'NONE', ( #2913, #2358, #3113, #89 ) ) ;
#3459=AXIS2_PLACEMENT_3D ( 'NONE', #5399, #7175, #6019 ) ;
#3463=EDGE_LOOP ( 'NONE', ( #463, #870, #1186, #5696 ) ) ;
#3501=CARTESIAN_POINT ( 'NONE',  ( 4.999999999999994671, 0.000000000000000000, 0.000000000000000000 ) ) ;
#3508=CARTESIAN_POINT ( 'NONE',  ( 10.40000000000000036, 0.000000000000000000, 0.000000000000000000 ) ) ;
#3522=PRODUCT_DEFINITION ( 'UNKNOWN', '', #2479, #6140 ) ;
#3575=ORIENTED_EDGE ( 'NONE', *, *, #1907, .F. ) ;
#3594=AXIS2_PLACEMENT_3D ( 'NONE', #3953, #4332, #5666 ) ;
#3599=EDGE_CURVE ( 'NONE', #6111, #6896, #649, .T. ) ;
#3620=CONICAL_SURFACE ( 'NONE', #3459, 4.057500000000000107, 1.047197551196592746 ) ;
#3640=DIRECTION ( 'NONE',  ( 0.000000000000000000, -0.5000000000000011102, -0.8660254037844379305 ) ) ;
#3651=EDGE_CURVE ( 'NONE', #5704, #7049, #695, .T. ) ;
#3663=ORIENTED_EDGE ( 'NONE', *, *, #1851, .F. ) ;
#3677=DIRECTION ( 'NONE',  ( 1.000000000000000000, 0.000000000000000000, 0.000000000000000000 ) ) ;
#3678=VERTEX_POINT ( 'NONE', #4087 ) ;
#3686=ORIENTED_EDGE ( 'NONE', *, *, #1335, .T. ) ;
#3702=CARTESIAN_POINT ( 'NONE',  ( 5.000000000000000000, 4.685197434473814759, -5.637851296924623057E-15 ) ) ;
#3720=( NAMED_UNIT ( * ) SI_UNIT ( $, .STERADIAN. ) SOLID_ANGLE_UNIT ( ) );
#3734=VECTOR ( 'NONE', #4438, 1000.000000000000114 ) ;
#3756=AXIS2_PLACEMENT_3D ( 'NONE', #4230, #2939, #4276 ) ;
#3766=AXIS2_PLACEMENT_3D ( 'NONE', #5567, #4916, #7506 ) ;
#3769=ORIENTED_EDGE ( 'NONE', *, *, #2764, .T. ) ;
#3808=VERTEX_POINT ( 'NONE', #4545 ) ;
#3819=( GEOMETRIC_REPRESENTATION_CONTEXT ( 3 ) GLOBAL_UNCERTAINTY_ASSIGNED_CONTEXT ( ( #1007 ) ) GLOBAL_UNIT_ASSIGNED_CONTEXT ( ( #7671, #3852, #6417 ) ) REPRESENTATION_CONTEXT ( 'NONE', 'WORKASPACE' ) );
#3825=EDGE_CURVE ( 'NONE', #2952, #7385, #6269, .T. ) ;
#3852=( NAMED_UNIT ( * ) PLANE_ANGLE_UNIT ( ) SI_UNIT ( $, .RADIAN. ) );
#3856=DIRECTION ( 'NONE',  ( -1.000000000000000000, -0.000000000000000000, -0.000000000000000000 ) ) ;
#3882=LINE ( 'NONE', #597, #1761 ) ;
#3885=ORIENTED_EDGE ( 'NONE', *, *, #6072, .F. ) ;
#3897=ORIENTED_EDGE ( 'NONE', *, *, #2452, .T. ) ;
#3900=CONICAL_SURFACE ( 'NONE', #7549, 6.999999999999999112, 0.7853981633974482790 ) ;
#3916=CARTESIAN_POINT ( 'NONE',  ( 0.000000000000000000, -2.342598717236898054, 4.057500000000003659 ) ) ;
#3927=ORIENTED_EDGE ( 'NONE', *, *, #5378, .F. ) ;
#3948=ORIENTED_EDGE ( 'NONE', *, *, #3376, .T. ) ;
#3949=CARTESIAN_POINT ( 'NONE',  ( 5.000000000000000000, 7.027796151710712813, -4.057500000000006324 ) ) ;
#3953=CARTESIAN_POINT ( 'NONE',  ( 5.000000000000000000, -2.342598717236898054, 4.057500000000003659 ) ) ;
#3954=EDGE_CURVE ( 'NONE', #5855, #7385, #4389, .T. ) ;
#3986=VERTEX_POINT ( 'NONE', #4216 ) ;
#3992=DIRECTION ( 'NONE',  ( -1.000000000000000000, -0.000000000000000000, -0.000000000000000000 ) ) ;
#3993=ORIENTED_EDGE ( 'NONE', *, *, #8247, .F. ) ;
#3995=VECTOR ( 'NONE', #5726, 1000.000000000000000 ) ;
#3998=ORIENTED_EDGE ( 'NONE', *, *, #980, .F. ) ;
#4003=AXIS2_PLACEMENT_3D ( 'NONE', #3508, #487, #6223 ) ;
#4016=PLANE ( 'NONE',  #5322 ) ;
#4029=PLANE ( 'NONE',  #2811 ) ;
#4032=AXIS2_PLACEMENT_3D ( 'NONE', #1778, #4127, #2785 ) ;
#4037=CARTESIAN_POINT ( 'NONE',  ( -31.74999999999995737, 9.797174393178825657E-16, -8.000000000000000000 ) ) ;
#4048=CARTESIAN_POINT ( 'NONE',  ( 0.000000000000000000, 9.184850993605147944E-16, 6.999999999999999112 ) ) ;
#4059=DIRECTION ( 'NONE',  ( 0.000000000000000000, 1.000000000000000000, -1.295896757998781966E-15 ) ) ;
#4065=CARTESIAN_POINT ( 'NONE',  ( 5.000000000000000000, -3.513898075855361292, -2.028749999999992504 ) ) ;
#4087=CARTESIAN_POINT ( 'NONE',  ( 1.000000000000000888, 0.000000000000000000, -8.000000000000000000 ) ) ;
#4098=CARTESIAN_POINT ( 'NONE',  ( 5.000000000000000000, 5.258101095580058680E-15, 4.057500000000000995 ) ) ;
#4106=FACE_OUTER_BOUND ( 'NONE', #6567, .T. ) ;
#4127=DIRECTION ( 'NONE',  ( 1.000000000000000000, 0.000000000000000000, 0.000000000000000000 ) ) ;
#4131=DIRECTION ( 'NONE',  ( -0.5000000000000042188, 0.000000000000000000, 0.8660254037844361541 ) ) ;
#4152=EDGE_CURVE ( 'NONE', #4329, #2735, #3294, .T. ) ;
#4161=AXIS2_PLACEMENT_3D ( 'NONE', #3288, #2017, #5800 ) ;
#4167=FACE_OUTER_BOUND ( 'NONE', #1883, .T. ) ;
#4168=CIRCLE ( 'NONE', #3357, 4.171999999999999709 ) ;
#4200=DIRECTION ( 'NONE',  ( 0.000000000000000000, 0.000000000000000000, 1.000000000000000000 ) ) ;
#4211=EDGE_CURVE ( 'NONE', #2952, #3213, #1982, .T. ) ;
#4213=EDGE_LOOP ( 'NONE', ( #6298, #5805 ) ) ;
#4216=CARTESIAN_POINT ( 'NONE',  ( 0.000000000000000000, -2.342598717236909600, -4.057499999999997442 ) ) ;
#4226=( GEOMETRIC_REPRESENTATION_CONTEXT ( 3 ) GLOBAL_UNCERTAINTY_ASSIGNED_CONTEXT ( ( #2850 ) ) GLOBAL_UNIT_ASSIGNED_CONTEXT ( ( #2311, #5131, #3720 ) ) REPRESENTATION_CONTEXT ( 'NONE', 'WORKASPACE' ) );
#4228=DIRECTION ( 'NONE',  ( 0.000000000000000000, 0.4999999999999984457, -0.8660254037844394848 ) ) ;
#4230=CARTESIAN_POINT ( 'NONE',  ( 5.000000000000000000, 7.027796151710712813, -4.057500000000006324 ) ) ;
#4243=VECTOR ( 'NONE', #1282, 1000.000000000000227 ) ;
#4266=EDGE_CURVE ( 'NONE', #6775, #6896, #6977, .T. ) ;
#4276=DIRECTION ( 'NONE',  ( 0.000000000000000000, 0.000000000000000000, -1.000000000000000000 ) ) ;
#4292=ORIENTED_EDGE ( 'NONE', *, *, #1907, .T. ) ;
#4308=CYLINDRICAL_SURFACE ( 'NONE', #6865, 5.000000000000035527 ) ;
#4309=ADVANCED_FACE ( 'NONE', ( #7993 ), #2232, .T. ) ;
#4323=CYLINDRICAL_SURFACE ( 'NONE', #5394, 8.000000000000000000 ) ;
#4327=CARTESIAN_POINT ( 'NONE',  ( 79.17200000000011073, 0.000000000000000000, 0.000000000000000000 ) ) ;
#4329=VERTEX_POINT ( 'NONE', #3407 ) ;
#4331=DIRECTION ( 'NONE',  ( 0.000000000000000000, 0.8660254037844380415, -0.5000000000000011102 ) ) ;
#4332=DIRECTION ( 'NONE',  ( -0.000000000000000000, 1.295896757998781966E-15, 1.000000000000000000 ) ) ;
#4334=DIRECTION ( 'NONE',  ( 0.000000000000000000, 1.000000000000000000, -1.295896757998781966E-15 ) ) ;
#4349=CARTESIAN_POINT ( 'NONE',  ( 5.000000000000000000, 2.342598717236902939, -4.057500000000001883 ) ) ;
#4358=EDGE_CURVE ( 'NONE', #4855, #1427, #4770, .T. ) ;
#4364=VECTOR ( 'NONE', #4059, 1000.000000000000000 ) ;
#4368=SHAPE_DEFINITION_REPRESENTATION ( #8091, #239 ) ;
#4389=LINE ( 'NONE', #4349, #1578 ) ;
#4401=CARTESIAN_POINT ( 'NONE',  ( 4.999999999999994671, -3.755786496842898268E-15, -4.057500000000000107 ) ) ;
#4435=VECTOR ( 'NONE', #7754, 1000.000000000000114 ) ;
#4438=DIRECTION ( 'NONE',  ( 0.000000000000000000, -0.4999999999999985012, 0.8660254037844393737 ) ) ;
#4445=ORIENTED_EDGE ( 'NONE', *, *, #5253, .T. ) ;
#4473=FACE_OUTER_BOUND ( 'NONE', #7698, .T. ) ;
#4487=ORIENTED_EDGE ( 'NONE', *, *, #2925, .T. ) ;
#4524=DIRECTION ( 'NONE',  ( 0.000000000000000000, 0.000000000000000000, -1.000000000000000000 ) ) ;
#4527=VECTOR ( 'NONE', #7067, 999.9999999999998863 ) ;
#4533=CARTESIAN_POINT ( 'NONE',  ( 9.999999999999998224, 0.000000000000000000, -5.400000000000035882 ) ) ;
#4545=CARTESIAN_POINT ( 'NONE',  ( 5.000000000000000000, -2.342598717236909600, -4.057499999999997442 ) ) ;
#4547=AXIS2_PLACEMENT_3D ( 'NONE', #4979, #4331, #511 ) ;
#4553=FACE_OUTER_BOUND ( 'NONE', #3463, .T. ) ;
#4557=LINE ( 'NONE', #81, #8085 ) ;
#4558=EDGE_LOOP ( 'NONE', ( #6348, #4709, #3264, #3575, #7411 ) ) ;
#4566=ORIENTED_EDGE ( 'NONE', *, *, #7822, .T. ) ;
#4593=LINE ( 'NONE', #3355, #4960 ) ;
#4630=CARTESIAN_POINT ( 'NONE',  ( 1.000000000000000888, 0.000000000000000000, 0.000000000000000000 ) ) ;
#4668=CARTESIAN_POINT ( 'NONE',  ( -31.74999999999995737, 0.000000000000000000, 5.000000000000035527 ) ) ;
#4700=DIRECTION ( 'NONE',  ( -1.000000000000000000, -0.000000000000000000, -0.000000000000000000 ) ) ;
#4709=ORIENTED_EDGE ( 'NONE', *, *, #5253, .F. ) ;
#4727=DIRECTION ( 'NONE',  ( -1.000000000000000000, -0.000000000000000000, -0.000000000000000000 ) ) ;
#4735=ORIENTED_EDGE ( 'NONE', *, *, #3236, .T. ) ;
#4749=CARTESIAN_POINT ( 'NONE',  ( 0.000000000000000000, 2.342598717236915373, 4.057499999999997442 ) ) ;
#4758=FACE_OUTER_BOUND ( 'NONE', #6514, .T. ) ;
#4759=ORIENTED_EDGE ( 'NONE', *, *, #1462, .F. ) ;
#4767=VERTEX_POINT ( 'NONE', #2061 ) ;
#4770=LINE ( 'NONE', #212, #5353 ) ;
#4771=CARTESIAN_POINT ( 'NONE',  ( 5.000000000000000000, 7.027796151710712813, -4.057500000000006324 ) ) ;
#4784=CARTESIAN_POINT ( 'NONE',  ( 5.000000000000000000, -3.513898075855354630, 2.028750000000002718 ) ) ;
#4796=EDGE_CURVE ( 'NONE', #6622, #2952, #6592, .T. ) ;
#4803=DIRECTION ( 'NONE',  ( -1.000000000000000000, -0.000000000000000000, -0.000000000000000000 ) ) ;
#4808=ORIENTED_EDGE ( 'NONE', *, *, #2335, .T. ) ;
#4811=AXIS2_PLACEMENT_3D ( 'NONE', #7441, #1651, #4200 ) ;
#4813=AXIS2_PLACEMENT_3D ( 'NONE', #3501, #5465, #8035 ) ;
#4817=EDGE_LOOP ( 'NONE', ( #8087, #935, #5598 ) ) ;
#4826=CARTESIAN_POINT ( 'NONE',  ( 5.000000000000000000, 2.342598717236902939, -4.057500000000001883 ) ) ;
#4829=CARTESIAN_POINT ( 'NONE',  ( 80.00000000000000000, 0.000000000000000000, 4.171999999999999709 ) ) ;
#4851=VERTEX_POINT ( 'NONE', #6756 ) ;
#4853=ORIENTED_EDGE ( 'NONE', *, *, #1136, .T. ) ;
#4855=VERTEX_POINT ( 'NONE', #6930 ) ;
#4856=VERTEX_POINT ( 'NONE', #5447 ) ;
#4888=EDGE_CURVE ( 'NONE', #1427, #1581, #6710, .T. ) ;
#4916=DIRECTION ( 'NONE',  ( -1.000000000000000000, -0.000000000000000000, -0.000000000000000000 ) ) ;
#4919=PLANE ( 'NONE',  #4032 ) ;
#4924=DIRECTION ( 'NONE',  ( -0.000000000000000000, 0.000000000000000000, 1.000000000000000000 ) ) ;
#4932=CARTESIAN_POINT ( 'NONE',  ( 0.000000000000000000, 0.000000000000000000, 0.000000000000000000 ) ) ;
#4938=CARTESIAN_POINT ( 'NONE',  ( 0.000000000000000000, -2.342598717236898054, 4.057500000000003659 ) ) ;
#4949=ADVANCED_FACE ( 'NONE', ( #5490, #2861 ), #2338, .T. ) ;
#4960=VECTOR ( 'NONE', #3992, 1000.000000000000000 ) ;
#4964=VECTOR ( 'NONE', #6958, 999.9999999999998863 ) ;
#4969=DIRECTION ( 'NONE',  ( -1.000000000000000000, -0.000000000000000000, -0.000000000000000000 ) ) ;
#4970=ORIENTED_EDGE ( 'NONE', *, *, #1136, .F. ) ;
#4979=CARTESIAN_POINT ( 'NONE',  ( 5.000000000000000000, 4.685197434473814759, -5.637851296924623057E-15 ) ) ;
#4985=ORIENTED_EDGE ( 'NONE', *, *, #7989, .F. ) ;
#4991=CARTESIAN_POINT ( 'NONE',  ( 5.000000000000000000, 2.342598717236902939, -4.057500000000001883 ) ) ;
#4995=EDGE_CURVE ( 'NONE', #1268, #4767, #92, .T. ) ;
#5000=CYLINDRICAL_SURFACE ( 'NONE', #6597, 8.000000000000000000 ) ;
#5019=ORIENTED_EDGE ( 'NONE', *, *, #7898, .F. ) ;
#5025=ORIENTED_EDGE ( 'NONE', *, *, #7844, .F. ) ;
#5030=EDGE_LOOP ( 'NONE', ( #6049, #3052, #2945, #2771, #3206 ) ) ;
#5050=CARTESIAN_POINT ( 'NONE',  ( 5.000000000000000000, 4.685197434473814759, -5.637851296924623057E-15 ) ) ;
#5054=EDGE_LOOP ( 'NONE', ( #1344, #6656, #5687, #7794, #1331 ) ) ;
#5089=VECTOR ( 'NONE', #7251, 1000.000000000000000 ) ;
#5108=AXIS2_PLACEMENT_3D ( 'NONE', #7676, #10, #2604 ) ;
#5131=( NAMED_UNIT ( * ) PLANE_ANGLE_UNIT ( ) SI_UNIT ( $, .RADIAN. ) );
#5157=ORIENTED_EDGE ( 'NONE', *, *, #4211, .T. ) ;
#5160=DIRECTION ( 'NONE',  ( 0.000000000000000000, 0.000000000000000000, -1.000000000000000000 ) ) ;
#5195=LINE ( 'NONE', #600, #7865 ) ;
#5246=LINE ( 'NONE', #7182, #6185 ) ;
#5253=EDGE_CURVE ( 'NONE', #6149, #3213, #4593, .T. ) ;
#5264=AXIS2_PLACEMENT_3D ( 'NONE', #1532, #4727, #5571 ) ;
#5279=ORIENTED_EDGE ( 'NONE', *, *, #7906, .T. ) ;
#5304=EDGE_LOOP ( 'NONE', ( #7488, #970, #1916, #2139, #4445 ) ) ;
#5311=DIRECTION ( 'NONE',  ( 1.000000000000000000, 0.000000000000000000, 0.000000000000000000 ) ) ;
#5322=AXIS2_PLACEMENT_3D ( 'NONE', #4771, #7235, #6644 ) ;
#5323=EDGE_CURVE ( 'NONE', #7049, #6111, #5438, .T. ) ;
#5348=DIRECTION ( 'NONE',  ( -0.000000000000000000, 0.8660254037844395958, 0.4999999999999985012 ) ) ;
#5353=VECTOR ( 'NONE', #4131, 1000.000000000000114 ) ;
#5367=CARTESIAN_POINT ( 'NONE',  ( 5.000000000000000000, -2.342598717236898054, 4.057500000000003659 ) ) ;
#5378=EDGE_CURVE ( 'NONE', #4856, #3986, #1603, .T. ) ;
#5394=AXIS2_PLACEMENT_3D ( 'NONE', #206, #4969, #6923 ) ;
#5399=CARTESIAN_POINT ( 'NONE',  ( 4.999999999999994671, 0.000000000000000000, 0.000000000000000000 ) ) ;
#5415=EDGE_CURVE ( 'NONE', #2791, #3078, #7402, .T. ) ;
#5416=EDGE_CURVE ( 'NONE', #1836, #6640, #939, .T. ) ;
#5427=APPLICATION_CONTEXT ( 'automotive_design' ) ;
#5430=ORIENTED_EDGE ( 'NONE', *, *, #767, .F. ) ;
#5438=LINE ( 'NONE', #6747, #8343 ) ;
#5447=CARTESIAN_POINT ( 'NONE',  ( 0.000000000000000000, -4.685197434473809430, 7.372574772901430151E-15 ) ) ;
#5463=EDGE_CURVE ( 'NONE', #2791, #8231, #800, .T. ) ;
#5465=DIRECTION ( 'NONE',  ( -1.000000000000000000, -0.000000000000000000, -0.000000000000000000 ) ) ;
#5467=CARTESIAN_POINT ( 'NONE',  ( 4.999999999999994671, 0.000000000000000000, 0.000000000000000000 ) ) ;
#5487=ORIENTED_EDGE ( 'NONE', *, *, #2764, .F. ) ;
#5488=CARTESIAN_POINT ( 'NONE',  ( 80.00000000000000000, 0.000000000000000000, 0.000000000000000000 ) ) ;
#5490=FACE_BOUND ( 'NONE', #234, .T. ) ;
#5491=FACE_OUTER_BOUND ( 'NONE', #7684, .T. ) ;
#5528=ADVANCED_BREP_SHAPE_REPRESENTATION ( '', ( #950, #1299 ), #3819 ) ;
#5532=CIRCLE ( 'NONE', #4161, 8.000000000000000000 ) ;
#5540=DIRECTION ( 'NONE',  ( 1.000000000000000000, 0.000000000000000000, 0.000000000000000000 ) ) ;
#5559=CARTESIAN_POINT ( 'NONE',  ( 5.000000000000000000, 3.513898075855358627, -2.028750000000004938 ) ) ;
#5562=EDGE_CURVE ( 'NONE', #6622, #1581, #2409, .T. ) ;
#5566=EDGE_LOOP ( 'NONE', ( #1870, #1376, #1329 ) ) ;
#5567=CARTESIAN_POINT ( 'NONE',  ( 0.000000000000000000, 0.000000000000000000, 0.000000000000000000 ) ) ;
#5571=DIRECTION ( 'NONE',  ( 0.000000000000000000, 0.000000000000000000, 1.000000000000000000 ) ) ;
#5595=DIRECTION ( 'NONE',  ( 0.000000000000000000, 1.224646799147353207E-16, 1.000000000000000000 ) ) ;
#5598=ORIENTED_EDGE ( 'NONE', *, *, #949, .F. ) ;
#5604=CARTESIAN_POINT ( 'NONE',  ( 0.000000000000000000, -4.685197434473809430, 7.372574772901430151E-15 ) ) ;
#5634=AXIS2_PLACEMENT_3D ( 'NONE', #7502, #7680, #1900 ) ;
#5637=CARTESIAN_POINT ( 'NONE',  ( -31.74999999999995737, 0.000000000000000000, 0.000000000000000000 ) ) ;
#5647=CARTESIAN_POINT ( 'NONE',  ( 5.000000000000000000, 4.685197434473814759, -5.637851296924623057E-15 ) ) ;
#5658=EDGE_LOOP ( 'NONE', ( #6206, #8260, #4759 ) ) ;
#5666=DIRECTION ( 'NONE',  ( 0.000000000000000000, -1.000000000000000000, 1.295896757998781966E-15 ) ) ;
#5674=ADVANCED_FACE ( 'NONE', ( #1425 ), #7889, .F. ) ;
#5687=ORIENTED_EDGE ( 'NONE', *, *, #3651, .T. ) ;
#5689=DIRECTION ( 'NONE',  ( -1.000000000000000000, -0.000000000000000000, -0.000000000000000000 ) ) ;
#5694=LINE ( 'NONE', #2576, #6585 ) ;
#5696=ORIENTED_EDGE ( 'NONE', *, *, #2335, .F. ) ;
#5704=VERTEX_POINT ( 'NONE', #5854 ) ;
#5717=CLOSED_SHELL ( 'NONE', ( #6538, #3232, #757, #7268, #7956, #6218, #1284, #6217, #6001, #4949, #562, #5863, #7015, #1305, #6063, #3103, #4309, #2381, #7267, #6334, #665, #2678, #6565, #7955, #5674, #7692, #6437 ) ) ;
#5726=DIRECTION ( 'NONE',  ( -1.000000000000000000, -0.000000000000000000, -0.000000000000000000 ) ) ;
#5758=ORIENTED_EDGE ( 'NONE', *, *, #7906, .F. ) ;
#5770=PLANE ( 'NONE',  #5634 ) ;
#5800=DIRECTION ( 'NONE',  ( 0.000000000000000000, 0.000000000000000000, 1.000000000000000000 ) ) ;
#5805=ORIENTED_EDGE ( 'NONE', *, *, #5416, .T. ) ;
#5822=AXIS2_PLACEMENT_3D ( 'NONE', #6137, #1638, #2810 ) ;
#5836=VECTOR ( 'NONE', #2453, 1000.000000000000114 ) ;
#5852=ORIENTED_EDGE ( 'NONE', *, *, #5463, .F. ) ;
#5854=CARTESIAN_POINT ( 'NONE',  ( 5.000000000000000000, -2.342598717236898054, 4.057500000000003659 ) ) ;
#5855=VERTEX_POINT ( 'NONE', #4826 ) ;
#5859=FACE_OUTER_BOUND ( 'NONE', #1201, .T. ) ;
#5863=ADVANCED_FACE ( 'NONE', ( #2356 ), #1611, .T. ) ;
#5884=CARTESIAN_POINT ( 'NONE',  ( 0.000000000000000000, 0.000000000000000000, 0.000000000000000000 ) ) ;
#5914=DIRECTION ( 'NONE',  ( 0.000000000000000000, 0.4999999999999984457, -0.8660254037844394848 ) ) ;
#5927=DIRECTION ( 'NONE',  ( 1.000000000000000000, 0.000000000000000000, 0.000000000000000000 ) ) ;
#5946=ORIENTED_EDGE ( 'NONE', *, *, #3651, .F. ) ;
#5957=CARTESIAN_POINT ( 'NONE',  ( 0.000000000000000000, 0.000000000000000000, -6.999999999999999112 ) ) ;
#5979=DIRECTION ( 'NONE',  ( -1.000000000000000000, -0.000000000000000000, -0.000000000000000000 ) ) ;
#5991=FACE_OUTER_BOUND ( 'NONE', #6851, .T. ) ;
#5994=DIRECTION ( 'NONE',  ( 0.7071067811865474617, 8.659560562354932858E-17, 0.7071067811865474617 ) ) ;
#5997=DIRECTION ( 'NONE',  ( 0.000000000000000000, 0.000000000000000000, 1.000000000000000000 ) ) ;
#5999=DIRECTION ( 'NONE',  ( -1.000000000000000000, -0.000000000000000000, -0.000000000000000000 ) ) ;
#6001=ADVANCED_FACE ( 'NONE', ( #4553 ), #5000, .T. ) ;
#6003=DIRECTION ( 'NONE',  ( -1.000000000000000000, -0.000000000000000000, -0.000000000000000000 ) ) ;
#6005=VERTEX_POINT ( 'NONE', #6261 ) ;
#6019=DIRECTION ( 'NONE',  ( 0.000000000000000000, 0.000000000000000000, 1.000000000000000000 ) ) ;
#6024=EDGE_CURVE ( 'NONE', #6622, #15, #5246, .T. ) ;
#6040=DIRECTION ( 'NONE',  ( 0.000000000000000000, 0.5000000000000011102, 0.8660254037844380415 ) ) ;
#6041=VECTOR ( 'NONE', #3305, 1000.000000000000114 ) ;
#6049=ORIENTED_EDGE ( 'NONE', *, *, #6750, .T. ) ;
#6051=DIRECTION ( 'NONE',  ( -1.000000000000000000, -0.000000000000000000, -0.000000000000000000 ) ) ;
#6063=ADVANCED_FACE ( 'NONE', ( #3008 ), #3051, .T. ) ;
#6072=EDGE_CURVE ( 'NONE', #4767, #2601, #249, .T. ) ;
#6077=CARTESIAN_POINT ( 'NONE',  ( 5.000000000000000000, -2.342598717236898054, 4.057500000000003659 ) ) ;
#6095=DIRECTION ( 'NONE',  ( 0.000000000000000000, 0.000000000000000000, 1.000000000000000000 ) ) ;
#6107=DIRECTION ( 'NONE',  ( 1.000000000000000000, 0.000000000000000000, 0.000000000000000000 ) ) ;
#6109=DIRECTION ( 'NONE',  ( 0.000000000000000000, 0.000000000000000000, -1.000000000000000000 ) ) ;
#6111=VERTEX_POINT ( 'NONE', #1529 ) ;
#6126=DIRECTION ( 'NONE',  ( 0.000000000000000000, 1.000000000000000000, -1.295896757998781966E-15 ) ) ;
#6137=CARTESIAN_POINT ( 'NONE',  ( 79.17200000000011073, 0.000000000000000000, 0.000000000000000000 ) ) ;
#6140=PRODUCT_DEFINITION_CONTEXT ( 'detailed design', #523, 'design' ) ;
#6149=VERTEX_POINT ( 'NONE', #7223 ) ;
#6159=VECTOR ( 'NONE', #6673, 1000.000000000000000 ) ;
#6174=VECTOR ( 'NONE', #3191, 1000.000000000000000 ) ;
#6179=ORIENTED_EDGE ( 'NONE', *, *, #2925, .F. ) ;
#6185=VECTOR ( 'NONE', #3640, 1000.000000000000114 ) ;
#6193=CARTESIAN_POINT ( 'NONE',  ( 0.000000000000000000, 0.000000000000000000, -6.999999999999999112 ) ) ;
#6206=ORIENTED_EDGE ( 'NONE', *, *, #5562, .F. ) ;
#6217=ADVANCED_FACE ( 'NONE', ( #4167 ), #3900, .T. ) ;
#6218=ADVANCED_FACE ( 'NONE', ( #5491 ), #250, .T. ) ;
#6223=DIRECTION ( 'NONE',  ( 0.000000000000000000, 0.000000000000000000, -1.000000000000000000 ) ) ;
#6233=ORIENTED_EDGE ( 'NONE', *, *, #6423, .T. ) ;
#6253=DIRECTION ( 'NONE',  ( 0.000000000000000000, 0.000000000000000000, -1.000000000000000000 ) ) ;
#6254=CONICAL_SURFACE ( 'NONE', #6530, 4.171999999999999709, 0.7853981633975609666 ) ;
#6261=CARTESIAN_POINT ( 'NONE',  ( 0.000000000000000000, -2.342598717236898054, 4.057500000000003659 ) ) ;
#6269=LINE ( 'NONE', #8233, #6972 ) ;
#6273=CARTESIAN_POINT ( 'NONE',  ( 0.000000000000000000, 2.342598717236902939, -4.057500000000001883 ) ) ;
#6279=DIRECTION ( 'NONE',  ( -1.000000000000000000, -0.000000000000000000, -0.000000000000000000 ) ) ;
#6281=DIRECTION ( 'NONE',  ( 1.000000000000000000, 0.000000000000000000, 0.000000000000000000 ) ) ;
#6298=ORIENTED_EDGE ( 'NONE', *, *, #1717, .T. ) ;
#6310=AXIS2_PLACEMENT_3D ( 'NONE', #3030, #4803, #1106 ) ;
#6332=AXIS2_PLACEMENT_3D ( 'NONE', #7521, #5540, #6109 ) ;
#6334=ADVANCED_FACE ( 'NONE', ( #2424 ), #1789, .F. ) ;
#6348=ORIENTED_EDGE ( 'NONE', *, *, #980, .T. ) ;
#6354=LINE ( 'NONE', #7072, #8316 ) ;
#6372=CARTESIAN_POINT ( 'NONE',  ( 5.000000000000000000, -2.342598717236898054, 4.057500000000003659 ) ) ;
#6384=ORIENTED_EDGE ( 'NONE', *, *, #1555, .T. ) ;
#6417=( NAMED_UNIT ( * ) SI_UNIT ( $, .STERADIAN. ) SOLID_ANGLE_UNIT ( ) );
#6423=EDGE_CURVE ( 'NONE', #3808, #3986, #3882, .T. ) ;
#6428=AXIS2_PLACEMENT_3D ( 'NONE', #1463, #7119, #4524 ) ;
#6437=ADVANCED_FACE ( 'NONE', ( #4758 ), #8230, .F. ) ;
#6439=LINE ( 'NONE', #3066, #4964 ) ;
#6462=AXIS2_PLACEMENT_3D ( 'NONE', #238, #2736, #1397 ) ;
#6483=FACE_OUTER_BOUND ( 'NONE', #683, .T. ) ;
#6488=EDGE_CURVE ( 'NONE', #1268, #3678, #2702, .T. ) ;
#6491=DIRECTION ( 'NONE',  ( 0.000000000000000000, 0.000000000000000000, -1.000000000000000000 ) ) ;
#6505=DIRECTION ( 'NONE',  ( -1.000000000000000000, -0.000000000000000000, -0.000000000000000000 ) ) ;
#6507=CARTESIAN_POINT ( 'NONE',  ( 9.999999999999998224, 0.000000000000000000, 0.000000000000000000 ) ) ;
#6514=EDGE_LOOP ( 'NONE', ( #5025, #7507, #2515, #7454, #4487 ) ) ;
#6530=AXIS2_PLACEMENT_3D ( 'NONE', #2847, #7380, #6776 ) ;
#6538=ADVANCED_FACE ( 'NONE', ( #846 ), #3620, .F. ) ;
#6551=LINE ( 'NONE', #5957, #4435 ) ;
#6565=ADVANCED_FACE ( 'NONE', ( #8052 ), #1681, .F. ) ;
#6567=EDGE_LOOP ( 'NONE', ( #7546, #6384, #5487, #8254 ) ) ;
#6577=CIRCLE ( 'NONE', #4003, 5.000000000000035527 ) ;
#6585=VECTOR ( 'NONE', #2617, 1000.000000000000000 ) ;
#6592=LINE ( 'NONE', #2739, #6159 ) ;
#6597=AXIS2_PLACEMENT_3D ( 'NONE', #5637, #6505, #7791 ) ;
#6617=ORIENTED_EDGE ( 'NONE', *, *, #1335, .F. ) ;
#6622=VERTEX_POINT ( 'NONE', #3702 ) ;
#6638=CARTESIAN_POINT ( 'NONE',  ( 0.000000000000000000, 8.572527594031472204E-16, 6.999999999999999112 ) ) ;
#6640=VERTEX_POINT ( 'NONE', #6193 ) ;
#6644=DIRECTION ( 'NONE',  ( 0.000000000000000000, 0.000000000000000000, -1.000000000000000000 ) ) ;
#6656=ORIENTED_EDGE ( 'NONE', *, *, #2649, .F. ) ;
#6673=DIRECTION ( 'NONE',  ( -1.000000000000000000, -0.000000000000000000, -0.000000000000000000 ) ) ;
#6710=CIRCLE ( 'NONE', #6310, 4.057500000000000107 ) ;
#6747=CARTESIAN_POINT ( 'NONE',  ( 5.000000000000000000, -2.342598717236898054, 4.057500000000003659 ) ) ;
#6750=EDGE_CURVE ( 'NONE', #7385, #3986, #8278, .T. ) ;
#6752=EDGE_CURVE ( 'NONE', #6111, #4856, #5694, .T. ) ;
#6756=CARTESIAN_POINT ( 'NONE',  ( 79.17200000000011073, 0.000000000000000000, 5.000000000000070166 ) ) ;
#6775=VERTEX_POINT ( 'NONE', #4401 ) ;
#6776=DIRECTION ( 'NONE',  ( 0.000000000000000000, 0.000000000000000000, 1.000000000000000000 ) ) ;
#6806=EDGE_CURVE ( 'NONE', #3292, #4851, #6439, .T. ) ;
#6851=EDGE_LOOP ( 'NONE', ( #3356, #456, #143, #3885 ) ) ;
#6859=DIRECTION ( 'NONE',  ( 0.000000000000000000, 1.000000000000000000, -1.224646799147353207E-16 ) ) ;
#6865=AXIS2_PLACEMENT_3D ( 'NONE', #6908, #4700, #5997 ) ;
#6876=EDGE_LOOP ( 'NONE', ( #5946, #4292, #1741 ) ) ;
#6896=VERTEX_POINT ( 'NONE', #4065 ) ;
#6908=CARTESIAN_POINT ( 'NONE',  ( -31.74999999999995737, 0.000000000000000000, 0.000000000000000000 ) ) ;
#6911=TOROIDAL_SURFACE ( 'NONE', #8268, 5.400000000000035882, 0.4000000000000000222 ) ;
#6923=DIRECTION ( 'NONE',  ( 0.000000000000000000, 0.000000000000000000, 1.000000000000000000 ) ) ;
#6925=PRODUCT_CONTEXT ( 'NONE', #5427, 'mechanical' ) ;
#6930=CARTESIAN_POINT ( 'NONE',  ( 7.342598717236928252, 0.000000000000000000, 0.000000000000000000 ) ) ;
#6936=AXIS2_PLACEMENT_3D ( 'NONE', #2727, #2200, #7247 ) ;
#6958=DIRECTION ( 'NONE',  ( -0.7071067811864679697, 0.000000000000000000, 0.7071067811866271757 ) ) ;
#6965=EDGE_CURVE ( 'NONE', #6005, #4856, #7928, .T. ) ;
#6971=DIRECTION ( 'NONE',  ( -1.000000000000000000, -0.000000000000000000, -0.000000000000000000 ) ) ;
#6972=VECTOR ( 'NONE', #7598, 1000.000000000000114 ) ;
#6977=CIRCLE ( 'NONE', #3193, 4.057500000000000107 ) ;
#6992=CARTESIAN_POINT ( 'NONE',  ( 5.000000000000000000, -2.342598717236898054, 4.057500000000003659 ) ) ;
#7007=ORIENTED_EDGE ( 'NONE', *, *, #5378, .T. ) ;
#7015=ADVANCED_FACE ( 'NONE', ( #6483 ), #4029, .T. ) ;
#7016=AXIS2_PLACEMENT_3D ( 'NONE', #6507, #3209, #5160 ) ;
#7049=VERTEX_POINT ( 'NONE', #4784 ) ;
#7067=DIRECTION ( 'NONE',  ( -0.7071067811864679697, 8.659560562355907841E-17, -0.7071067811866271757 ) ) ;
#7070=FACE_OUTER_BOUND ( 'NONE', #5030, .T. ) ;
#7072=CARTESIAN_POINT ( 'NONE',  ( 5.000000000000000000, 4.685197434473814759, -5.637851296924623057E-15 ) ) ;
#7076=ORIENTED_EDGE ( 'NONE', *, *, #4358, .F. ) ;
#7119=DIRECTION ( 'NONE',  ( -1.000000000000000000, -0.000000000000000000, -0.000000000000000000 ) ) ;
#7123=CIRCLE ( 'NONE', #4813, 4.057500000000000107 ) ;
#7175=DIRECTION ( 'NONE',  ( -1.000000000000000000, -0.000000000000000000, -0.000000000000000000 ) ) ;
#7182=CARTESIAN_POINT ( 'NONE',  ( 5.000000000000000000, 4.685197434473814759, -5.637851296924623057E-15 ) ) ;
#7185=CARTESIAN_POINT ( 'NONE',  ( 0.000000000000000000, 4.685197434473814759, -5.637851296924623057E-15 ) ) ;
#7212=DIRECTION ( 'NONE',  ( 0.000000000000000000, 0.000000000000000000, 1.000000000000000000 ) ) ;
#7223=CARTESIAN_POINT ( 'NONE',  ( 5.000000000000000000, 2.342598717236915373, 4.057499999999997442 ) ) ;
#7235=DIRECTION ( 'NONE',  ( 1.000000000000000000, 0.000000000000000000, 0.000000000000000000 ) ) ;
#7247=DIRECTION ( 'NONE',  ( 0.000000000000000000, 0.000000000000000000, 1.000000000000000000 ) ) ;
#7251=DIRECTION ( 'NONE',  ( -1.000000000000000000, -0.000000000000000000, -0.000000000000000000 ) ) ;
#7252=AXIS2_PLACEMENT_3D ( 'NONE', #978, #6107, #328 ) ;
#7265=AXIS2_PLACEMENT_3D ( 'NONE', #1905, #1179, #626 ) ;
#7267=ADVANCED_FACE ( 'NONE', ( #7070 ), #2520, .F. ) ;
#7268=ADVANCED_FACE ( 'NONE', ( #1769 ), #4308, .T. ) ;
#7284=FACE_OUTER_BOUND ( 'NONE', #8223, .T. ) ;
#7288=CARTESIAN_POINT ( 'NONE',  ( 5.000000000000000000, -2.342598717236898054, 4.057500000000003659 ) ) ;
#7289=CARTESIAN_POINT ( 'NONE',  ( 10.40000000000000036, 6.123233995736809670E-16, -5.000000000000035527 ) ) ;
#7290=ORIENTED_EDGE ( 'NONE', *, *, #2196, .T. ) ;
#7309=CARTESIAN_POINT ( 'NONE',  ( -31.74999999999995737, 0.000000000000000000, 8.000000000000000000 ) ) ;
#7311=CIRCLE ( 'NONE', #2730, 5.000000000000070166 ) ;
#7330=DIRECTION ( 'NONE',  ( 0.000000000000000000, 0.000000000000000000, 1.000000000000000000 ) ) ;
#7342=ORIENTED_EDGE ( 'NONE', *, *, #6024, .F. ) ;
#7355=STYLED_ITEM('',(#8407),#950);
#7380=DIRECTION ( 'NONE',  ( -1.000000000000000000, -0.000000000000000000, -0.000000000000000000 ) ) ;
#7385=VERTEX_POINT ( 'NONE', #213 ) ;
#7402=CIRCLE ( 'NONE', #656, 0.4000000000000001887 ) ;
#7408=AXIS2_PLACEMENT_3D ( 'NONE', #1713, #6051, #7330 ) ;
#7411=ORIENTED_EDGE ( 'NONE', *, *, #2649, .T. ) ;
#7427=PRODUCT ( 'socket head cap screw_am_B18.3.1M - 10 x 1.5 x 70 Hex SHCS -- 32NHX', 'socket head cap screw_am_B18.3.1M - 10 x 1.5 x 70 Hex SHCS -- 32NHX', '', ( #6925 ) ) ;
#7441=CARTESIAN_POINT ( 'NONE',  ( 9.999999999999994671, 0.000000000000000000, 0.000000000000000000 ) ) ;
#7454=ORIENTED_EDGE ( 'NONE', *, *, #1462, .T. ) ;
#7488=ORIENTED_EDGE ( 'NONE', *, *, #4211, .F. ) ;
#7502=CARTESIAN_POINT ( 'NONE',  ( 5.000000000000000000, 7.027796151710712813, -4.057500000000006324 ) ) ;
#7506=DIRECTION ( 'NONE',  ( 0.000000000000000000, 0.000000000000000000, 1.000000000000000000 ) ) ;
#7507=ORIENTED_EDGE ( 'NONE', *, *, #4358, .T. ) ;
#7514=DIRECTION ( 'NONE',  ( 0.000000000000000000, 0.000000000000000000, 1.000000000000000000 ) ) ;
#7521=CARTESIAN_POINT ( 'NONE',  ( 0.000000000000000000, 0.000000000000000000, 0.000000000000000000 ) ) ;
#7543=VECTOR ( 'NONE', #1138, 1000.000000000000114 ) ;
#7546=ORIENTED_EDGE ( 'NONE', *, *, #3253, .F. ) ;
#7549=AXIS2_PLACEMENT_3D ( 'NONE', #4932, #981, #2949 ) ;
#7554=VECTOR ( 'NONE', #2662, 1000.000000000000000 ) ;
#7558=ORIENTED_EDGE ( 'NONE', *, *, #3954, .F. ) ;
#7582=AXIS2_PLACEMENT_3D ( 'NONE', #4630, #146, #7212 ) ;
#7583=SHAPE_REPRESENTATION_RELATIONSHIP ( 'NONE' , 'NONE' ,  #239, #5528 ) ;
#7598=DIRECTION ( 'NONE',  ( 0.000000000000000000, -0.5000000000000011102, -0.8660254037844379305 ) ) ;
#7620=LINE ( 'NONE', #4991, #8229 ) ;
#7633=LINE ( 'NONE', #6992, #3995 ) ;
#7671=( LENGTH_UNIT ( ) NAMED_UNIT ( * ) SI_UNIT ( .MILLI., .METRE. ) );
#7676=CARTESIAN_POINT ( 'NONE',  ( 5.000000000000000000, 2.342598717236902939, -4.057500000000001883 ) ) ;
#7680=DIRECTION ( 'NONE',  ( 1.000000000000000000, 0.000000000000000000, 0.000000000000000000 ) ) ;
#7684=EDGE_LOOP ( 'NONE', ( #2943, #7863, #4566, #5758 ) ) ;
#7692=ADVANCED_FACE ( 'NONE', ( #4473 ), #1119, .F. ) ;
#7698=EDGE_LOOP ( 'NONE', ( #2253, #3330, #6179 ) ) ;
#7732=EDGE_LOOP ( 'NONE', ( #4970, #3686, #4735, #332 ) ) ;
#7745=EDGE_CURVE ( 'NONE', #5855, #6775, #7620, .T. ) ;
#7750=EDGE_LOOP ( 'NONE', ( #3897, #4853, #2039, #1307 ) ) ;
#7754=DIRECTION ( 'NONE',  ( 0.7071067811865474617, 0.000000000000000000, -0.7071067811865474617 ) ) ;
#7762=AXIS2_PLACEMENT_3D ( 'NONE', #1516, #5979, #6095 ) ;
#7791=DIRECTION ( 'NONE',  ( 0.000000000000000000, 0.000000000000000000, 1.000000000000000000 ) ) ;
#7794=ORIENTED_EDGE ( 'NONE', *, *, #5323, .T. ) ;
#7818=FACE_OUTER_BOUND ( 'NONE', #4558, .T. ) ;
#7822=EDGE_CURVE ( 'NONE', #2601, #3678, #5532, .T. ) ;
#7844=EDGE_CURVE ( 'NONE', #4855, #6775, #2065, .T. ) ;
#7854=EDGE_CURVE ( 'NONE', #6896, #3808, #4557, .T. ) ;
#7857=CARTESIAN_POINT ( 'NONE',  ( 10.40000000000000036, 0.000000000000000000, 0.000000000000000000 ) ) ;
#7863=ORIENTED_EDGE ( 'NONE', *, *, #1851, .T. ) ;
#7865=VECTOR ( 'NONE', #8330, 1000.000000000000000 ) ;
#7889=PLANE ( 'NONE',  #1339 ) ;
#7898=EDGE_CURVE ( 'NONE', #1537, #3078, #540, .T. ) ;
#7906=EDGE_CURVE ( 'NONE', #6640, #3678, #6551, .T. ) ;
#7913=DIRECTION ( 'NONE',  ( 0.000000000000000000, -0.5000000000000011102, -0.8660254037844379305 ) ) ;
#7927=CIRCLE ( 'NONE', #6428, 5.400000000000035882 ) ;
#7928=LINE ( 'NONE', #3916, #6041 ) ;
#7955=ADVANCED_FACE ( 'NONE', ( #1099 ), #4919, .F. ) ;
#7956=ADVANCED_FACE ( 'NONE', ( #5991 ), #4323, .T. ) ;
#7966=FACE_OUTER_BOUND ( 'NONE', #7732, .T. ) ;
#7989=EDGE_CURVE ( 'NONE', #4767, #1268, #3225, .T. ) ;
#7993=FACE_OUTER_BOUND ( 'NONE', #5054, .T. ) ;
#8005=DIRECTION ( 'NONE',  ( 0.000000000000000000, 0.000000000000000000, -1.000000000000000000 ) ) ;
#8035=DIRECTION ( 'NONE',  ( 0.000000000000000000, 0.000000000000000000, 1.000000000000000000 ) ) ;
#8052=FACE_OUTER_BOUND ( 'NONE', #6876, .T. ) ;
#8083=DIRECTION ( 'NONE',  ( -1.000000000000000000, -0.000000000000000000, -0.000000000000000000 ) ) ;
#8085=VECTOR ( 'NONE', #5914, 1000.000000000000227 ) ;
#8087=ORIENTED_EDGE ( 'NONE', *, *, #3599, .F. ) ;
#8091=PRODUCT_DEFINITION_SHAPE ( 'NONE', 'NONE',  #3522 ) ;
#8133=ORIENTED_EDGE ( 'NONE', *, *, #4995, .F. ) ;
#8149=DIRECTION ( 'NONE',  ( -1.000000000000000000, 0.000000000000000000, -0.000000000000000000 ) ) ;
#8158=ORIENTED_EDGE ( 'NONE', *, *, #4266, .T. ) ;
#8159=CIRCLE ( 'NONE', #7762, 4.171999999999999709 ) ;
#8184=CARTESIAN_POINT ( 'NONE',  ( 10.40000000000000036, 0.000000000000000000, -5.400000000000035882 ) ) ;
#8213=CARTESIAN_POINT ( 'NONE',  ( 5.000000000000000000, 7.027796151710712813, -4.057500000000006324 ) ) ;
#8223=EDGE_LOOP ( 'NONE', ( #3948, #414, #1241 ) ) ;
#8229=VECTOR ( 'NONE', #1841, 1000.000000000000000 ) ;
#8230=CONICAL_SURFACE ( 'NONE', #6462, 4.057500000000000107, 1.047197551196592746 ) ;
#8231=VERTEX_POINT ( 'NONE', #1941 ) ;
#8233=CARTESIAN_POINT ( 'NONE',  ( 0.000000000000000000, 4.685197434473814759, -5.637851296924623057E-15 ) ) ;
#8247=EDGE_CURVE ( 'NONE', #15, #5855, #6354, .T. ) ;
#8251=LINE ( 'NONE', #4938, #1688 ) ;
#8254=ORIENTED_EDGE ( 'NONE', *, *, #5415, .F. ) ;
#8260=ORIENTED_EDGE ( 'NONE', *, *, #6024, .T. ) ;
#8261=CARTESIAN_POINT ( 'NONE',  ( 5.000000000000000000, 3.513898075855365732, 2.028749999999995612 ) ) ;
#8268=AXIS2_PLACEMENT_3D ( 'NONE', #1147, #6281, #6491 ) ;
#8272=DIRECTION ( 'NONE',  ( -1.000000000000000000, -0.000000000000000000, -0.000000000000000000 ) ) ;
#8278=LINE ( 'NONE', #6273, #6174 ) ;
#8316=VECTOR ( 'NONE', #12, 1000.000000000000114 ) ;
#8317=ORIENTED_EDGE ( 'NONE', *, *, #6752, .F. ) ;
#8330=DIRECTION ( 'NONE',  ( -1.000000000000000000, -0.000000000000000000, -0.000000000000000000 ) ) ;
#8343=VECTOR ( 'NONE', #2327, 1000.000000000000114 ) ;
#8347=LINE ( 'NONE', #6372, #793 ) ;
#8401=COLOUR_RGB('Black',0.12,0.14,0.17);
#8402=FILL_AREA_STYLE_COLOUR('',#8401);
#8403=FILL_AREA_STYLE('',(#8402));
#8404=SURFACE_STYLE_FILL_AREA(#8403);
#8405=SURFACE_SIDE_STYLE('',(#8404));
#8406=SURFACE_STYLE_USAGE(.BOTH.,#8405);
#8407=PRESENTATION_STYLE_ASSIGNMENT((#8406));
ENDSEC;
END-ISO-10303-21;
